ISO-10303-21;
HEADER;
/* Generated by software containing ST-Developer
 * from STEP Tools, Inc. (www.steptools.com) 
 */
/* OPTION: using custom renumber hook */

FILE_DESCRIPTION(
/* description */ ('STEP AP242 Edition 2', 'CAx-IF Rec.Pracs.---Representation and Presentation of Product Manufa
cturing Information (PMI)---4.0---2014-10-13', 'CAx-IF Rec.Pracs.---3D Tessellated Geometry---0.4---2014-09-14', '2;1', 'CAx-IF Rec.Pracs.---User Defined Attributes---1.5---2016-08-15'),
/* implementation_level */ '2;1');

FILE_NAME(
/* name */ 'refill+port_air_seal.step',
/* time_stamp */ '2026-10-08T12:15:07Z',
/* author */ (''),
/* organization */ (''),
/* preprocessor_version */ 'ST-DEVELOPER v20',
/* originating_system */ 'ONSHAPE BY PTC INC, 1.221',
/* authorisation */ '  ');

FILE_SCHEMA (('AP242_MANAGED_MODEL_BASED_3D_ENGINEERING_MIM_LF { 1 0 10303 442 3 1 4 }'));
ENDSEC;

DATA;
#60=COLOUR_RGB('', 0.66274510, 0.83137255, 0.94901961);
#220=SHAPE_REPRESENTATION_RELATIONSHIP('','',#13794,#247);
#247=ADVANCED_BREP_SHAPE_REPRESENTATION('',(#13738),#45484);
#823=CIRCLE('',#14806,0.000477030566374308);
#824=CIRCLE('',#14807,0.00322703056637436);
#825=CIRCLE('',#14808,0.000477030566374308);
#826=CIRCLE('',#14809,0.00227296943362574);
#827=CIRCLE('',#14811,0.000477030566374308);
#828=CIRCLE('',#14813,0.000477030566374308);
#829=CIRCLE('',#14815,0.000477030566374308);
#830=CIRCLE('',#14816,0.00227296943362564);
#831=CIRCLE('',#14817,0.000477030566374308);
#832=CIRCLE('',#14818,0.00322703056637426);
#833=CIRCLE('',#14820,0.00322703056637426);
#834=CIRCLE('',#14822,0.00227296943362564);
#835=CIRCLE('',#14824,0.001);
#836=CIRCLE('',#14825,0.0035);
#837=CIRCLE('',#14826,0.001);
#838=CIRCLE('',#14827,0.0035);
#839=CIRCLE('',#14829,0.001);
#840=CIRCLE('',#14831,0.0035);
#841=CIRCLE('',#14832,0.001);
#842=CIRCLE('',#14833,0.000477030566374308);
#843=CIRCLE('',#14834,0.000477030566374308);
#844=CIRCLE('',#14836,0.0035);
#845=CIRCLE('',#14838,0.001);
#846=CIRCLE('',#14839,0.00322703056637436);
#847=CIRCLE('',#14840,0.00227296943362574);
#1423=PLANE('',#14801);
#1424=PLANE('',#14802);
#1425=PLANE('',#14803);
#1426=PLANE('',#14804);
#1427=PLANE('',#14805);
#1428=PLANE('',#14814);
#1429=PLANE('',#14823);
#1430=PLANE('',#14828);
#1431=PLANE('',#14830);
#1432=PLANE('',#14837);
#1725=CYLINDRICAL_SURFACE('',#14810,0.000477030566374308);
#1726=CYLINDRICAL_SURFACE('',#14812,0.000477030566374308);
#1727=CYLINDRICAL_SURFACE('',#14819,0.00322703056637436);
#1728=CYLINDRICAL_SURFACE('',#14821,0.00227296943362574);
#1729=CYLINDRICAL_SURFACE('',#14835,0.0035);
#1730=CYLINDRICAL_SURFACE('',#14841,0.001);
#1731=CYLINDRICAL_SURFACE('',#14842,0.0035);
#1732=CYLINDRICAL_SURFACE('',#14843,0.000477030566374308);
#1733=CYLINDRICAL_SURFACE('',#14844,0.000477030566374308);
#1734=CYLINDRICAL_SURFACE('',#14845,0.00322703056637436);
#1735=CYLINDRICAL_SURFACE('',#14846,0.00227296943362574);
#4264=ORIENTED_EDGE('',*,*,#6779,.T.);
#4265=ORIENTED_EDGE('',*,*,#6780,.T.);
#4266=ORIENTED_EDGE('',*,*,#6781,.T.);
#4267=ORIENTED_EDGE('',*,*,#6782,.F.);
#4268=ORIENTED_EDGE('',*,*,#6783,.T.);
#4269=ORIENTED_EDGE('',*,*,#6784,.T.);
#4270=ORIENTED_EDGE('',*,*,#6785,.T.);
#4271=ORIENTED_EDGE('',*,*,#6786,.F.);
#4272=ORIENTED_EDGE('',*,*,#6787,.T.);
#4273=ORIENTED_EDGE('',*,*,#6788,.T.);
#4274=ORIENTED_EDGE('',*,*,#6789,.T.);
#4275=ORIENTED_EDGE('',*,*,#6790,.F.);
#4276=ORIENTED_EDGE('',*,*,#6791,.T.);
#4277=ORIENTED_EDGE('',*,*,#6792,.T.);
#4278=ORIENTED_EDGE('',*,*,#6793,.T.);
#4279=ORIENTED_EDGE('',*,*,#6794,.F.);
#4280=ORIENTED_EDGE('',*,*,#6795,.F.);
#4281=ORIENTED_EDGE('',*,*,#6796,.F.);
#4282=ORIENTED_EDGE('',*,*,#6797,.F.);
#4283=ORIENTED_EDGE('',*,*,#6798,.F.);
#4284=ORIENTED_EDGE('',*,*,#6799,.F.);
#4285=ORIENTED_EDGE('',*,*,#6800,.F.);
#4286=ORIENTED_EDGE('',*,*,#6797,.T.);
#4287=ORIENTED_EDGE('',*,*,#6801,.T.);
#4288=ORIENTED_EDGE('',*,*,#6802,.F.);
#4289=ORIENTED_EDGE('',*,*,#6803,.F.);
#4290=ORIENTED_EDGE('',*,*,#6795,.T.);
#4291=ORIENTED_EDGE('',*,*,#6804,.T.);
#4292=ORIENTED_EDGE('',*,*,#6805,.F.);
#4293=ORIENTED_EDGE('',*,*,#6806,.F.);
#4294=ORIENTED_EDGE('',*,*,#6807,.F.);
#4295=ORIENTED_EDGE('',*,*,#6808,.F.);
#4296=ORIENTED_EDGE('',*,*,#6809,.F.);
#4297=ORIENTED_EDGE('',*,*,#6810,.F.);
#4298=ORIENTED_EDGE('',*,*,#6808,.T.);
#4299=ORIENTED_EDGE('',*,*,#6811,.T.);
#4300=ORIENTED_EDGE('',*,*,#6812,.F.);
#4301=ORIENTED_EDGE('',*,*,#6813,.F.);
#4302=ORIENTED_EDGE('',*,*,#6806,.T.);
#4303=ORIENTED_EDGE('',*,*,#6814,.T.);
#4304=ORIENTED_EDGE('',*,*,#6783,.F.);
#4305=ORIENTED_EDGE('',*,*,#6815,.F.);
#4306=ORIENTED_EDGE('',*,*,#6779,.F.);
#4307=ORIENTED_EDGE('',*,*,#6816,.T.);
#4308=ORIENTED_EDGE('',*,*,#6791,.F.);
#4309=ORIENTED_EDGE('',*,*,#6817,.F.);
#4310=ORIENTED_EDGE('',*,*,#6787,.F.);
#4311=ORIENTED_EDGE('',*,*,#6818,.T.);
#4312=ORIENTED_EDGE('',*,*,#6819,.F.);
#4313=ORIENTED_EDGE('',*,*,#6820,.F.);
#4314=ORIENTED_EDGE('',*,*,#6781,.F.);
#4315=ORIENTED_EDGE('',*,*,#6821,.T.);
#4316=ORIENTED_EDGE('',*,*,#6793,.F.);
#4317=ORIENTED_EDGE('',*,*,#6812,.T.);
#4318=ORIENTED_EDGE('',*,*,#6822,.T.);
#4319=ORIENTED_EDGE('',*,*,#6809,.T.);
#4320=ORIENTED_EDGE('',*,*,#6823,.T.);
#4321=ORIENTED_EDGE('',*,*,#6824,.T.);
#4322=ORIENTED_EDGE('',*,*,#6784,.F.);
#4323=ORIENTED_EDGE('',*,*,#6818,.F.);
#4324=ORIENTED_EDGE('',*,*,#6790,.T.);
#4325=ORIENTED_EDGE('',*,*,#6789,.F.);
#4326=ORIENTED_EDGE('',*,*,#6825,.T.);
#4327=ORIENTED_EDGE('',*,*,#6785,.F.);
#4328=ORIENTED_EDGE('',*,*,#6824,.F.);
#4329=ORIENTED_EDGE('',*,*,#6826,.T.);
#4330=ORIENTED_EDGE('',*,*,#6802,.T.);
#4331=ORIENTED_EDGE('',*,*,#6827,.T.);
#4332=ORIENTED_EDGE('',*,*,#6799,.T.);
#4333=ORIENTED_EDGE('',*,*,#6825,.F.);
#4334=ORIENTED_EDGE('',*,*,#6788,.F.);
#4335=ORIENTED_EDGE('',*,*,#6817,.T.);
#4336=ORIENTED_EDGE('',*,*,#6794,.T.);
#4337=ORIENTED_EDGE('',*,*,#6821,.F.);
#4338=ORIENTED_EDGE('',*,*,#6780,.F.);
#4339=ORIENTED_EDGE('',*,*,#6815,.T.);
#4340=ORIENTED_EDGE('',*,*,#6786,.T.);
#4341=ORIENTED_EDGE('',*,*,#6819,.T.);
#4342=ORIENTED_EDGE('',*,*,#6816,.F.);
#4343=ORIENTED_EDGE('',*,*,#6782,.T.);
#4344=ORIENTED_EDGE('',*,*,#6820,.T.);
#4345=ORIENTED_EDGE('',*,*,#6792,.F.);
#4346=ORIENTED_EDGE('',*,*,#6805,.T.);
#4347=ORIENTED_EDGE('',*,*,#6810,.T.);
#4348=ORIENTED_EDGE('',*,*,#6822,.F.);
#4349=ORIENTED_EDGE('',*,*,#6814,.F.);
#4350=ORIENTED_EDGE('',*,*,#6807,.T.);
#4351=ORIENTED_EDGE('',*,*,#6813,.T.);
#4352=ORIENTED_EDGE('',*,*,#6823,.F.);
#4353=ORIENTED_EDGE('',*,*,#6811,.F.);
#4354=ORIENTED_EDGE('',*,*,#6796,.T.);
#4355=ORIENTED_EDGE('',*,*,#6803,.T.);
#4356=ORIENTED_EDGE('',*,*,#6826,.F.);
#4357=ORIENTED_EDGE('',*,*,#6801,.F.);
#4358=ORIENTED_EDGE('',*,*,#6798,.T.);
#4359=ORIENTED_EDGE('',*,*,#6800,.T.);
#4360=ORIENTED_EDGE('',*,*,#6827,.F.);
#4361=ORIENTED_EDGE('',*,*,#6804,.F.);
#6779=EDGE_CURVE('',#8286,#8287,#9303,.T.);
#6780=EDGE_CURVE('',#8287,#8288,#9304,.T.);
#6781=EDGE_CURVE('',#8288,#8289,#9305,.T.);
#6782=EDGE_CURVE('',#8286,#8289,#9306,.T.);
#6783=EDGE_CURVE('',#8290,#8291,#9307,.T.);
#6784=EDGE_CURVE('',#8291,#8292,#9308,.T.);
#6785=EDGE_CURVE('',#8292,#8293,#9309,.T.);
#6786=EDGE_CURVE('',#8290,#8293,#9310,.T.);
#6787=EDGE_CURVE('',#8294,#8295,#9311,.T.);
#6788=EDGE_CURVE('',#8295,#8296,#9312,.T.);
#6789=EDGE_CURVE('',#8296,#8297,#9313,.T.);
#6790=EDGE_CURVE('',#8294,#8297,#9314,.T.);
#6791=EDGE_CURVE('',#8298,#8299,#9315,.T.);
#6792=EDGE_CURVE('',#8299,#8300,#9316,.T.);
#6793=EDGE_CURVE('',#8300,#8301,#9317,.T.);
#6794=EDGE_CURVE('',#8298,#8301,#9318,.T.);
#6795=EDGE_CURVE('',#8302,#8303,#823,.T.);
#6796=EDGE_CURVE('',#8304,#8302,#824,.T.);
#6797=EDGE_CURVE('',#8305,#8304,#825,.T.);
#6798=EDGE_CURVE('',#8303,#8305,#826,.T.);
#6799=EDGE_CURVE('',#8306,#8307,#827,.T.);
#6800=EDGE_CURVE('',#8305,#8306,#9319,.T.);
#6801=EDGE_CURVE('',#8304,#8307,#9320,.T.);
#6802=EDGE_CURVE('',#8308,#8309,#828,.T.);
#6803=EDGE_CURVE('',#8302,#8308,#9321,.T.);
#6804=EDGE_CURVE('',#8303,#8309,#9322,.T.);
#6805=EDGE_CURVE('',#8310,#8311,#829,.T.);
#6806=EDGE_CURVE('',#8312,#8310,#830,.T.);
#6807=EDGE_CURVE('',#8313,#8312,#831,.T.);
#6808=EDGE_CURVE('',#8311,#8313,#832,.T.);
#6809=EDGE_CURVE('',#8314,#8315,#833,.T.);
#6810=EDGE_CURVE('',#8311,#8314,#9323,.T.);
#6811=EDGE_CURVE('',#8313,#8315,#9324,.T.);
#6812=EDGE_CURVE('',#8316,#8317,#834,.T.);
#6813=EDGE_CURVE('',#8312,#8316,#9325,.T.);
#6814=EDGE_CURVE('',#8310,#8317,#9326,.T.);
#6815=EDGE_CURVE('',#8287,#8290,#835,.T.);
#6816=EDGE_CURVE('',#8286,#8299,#836,.T.);
#6817=EDGE_CURVE('',#8295,#8298,#837,.T.);
#6818=EDGE_CURVE('',#8294,#8291,#838,.T.);
#6819=EDGE_CURVE('',#8318,#8318,#839,.T.);
#6820=EDGE_CURVE('',#8289,#8300,#840,.T.);
#6821=EDGE_CURVE('',#8288,#8301,#841,.T.);
#6822=EDGE_CURVE('',#8317,#8314,#842,.T.);
#6823=EDGE_CURVE('',#8315,#8316,#843,.T.);
#6824=EDGE_CURVE('',#8297,#8292,#844,.T.);
#6825=EDGE_CURVE('',#8296,#8293,#845,.T.);
#6826=EDGE_CURVE('',#8307,#8308,#846,.T.);
#6827=EDGE_CURVE('',#8309,#8306,#847,.T.);
#8286=VERTEX_POINT('',#35275);
#8287=VERTEX_POINT('',#35276);
#8288=VERTEX_POINT('',#35278);
#8289=VERTEX_POINT('',#35280);
#8290=VERTEX_POINT('',#35284);
#8291=VERTEX_POINT('',#35285);
#8292=VERTEX_POINT('',#35287);
#8293=VERTEX_POINT('',#35289);
#8294=VERTEX_POINT('',#35293);
#8295=VERTEX_POINT('',#35294);
#8296=VERTEX_POINT('',#35296);
#8297=VERTEX_POINT('',#35298);
#8298=VERTEX_POINT('',#35302);
#8299=VERTEX_POINT('',#35303);
#8300=VERTEX_POINT('',#35305);
#8301=VERTEX_POINT('',#35307);
#8302=VERTEX_POINT('',#35311);
#8303=VERTEX_POINT('',#35312);
#8304=VERTEX_POINT('',#35314);
#8305=VERTEX_POINT('',#35316);
#8306=VERTEX_POINT('',#35320);
#8307=VERTEX_POINT('',#35321);
#8308=VERTEX_POINT('',#35326);
#8309=VERTEX_POINT('',#35327);
#8310=VERTEX_POINT('',#35332);
#8311=VERTEX_POINT('',#35333);
#8312=VERTEX_POINT('',#35335);
#8313=VERTEX_POINT('',#35337);
#8314=VERTEX_POINT('',#35341);
#8315=VERTEX_POINT('',#35342);
#8316=VERTEX_POINT('',#35347);
#8317=VERTEX_POINT('',#35348);
#8318=VERTEX_POINT('',#35358);
#9303=LINE('',#35274,#10131);
#9304=LINE('',#35277,#10132);
#9305=LINE('',#35279,#10133);
#9306=LINE('',#35281,#10134);
#9307=LINE('',#35283,#10135);
#9308=LINE('',#35286,#10136);
#9309=LINE('',#35288,#10137);
#9310=LINE('',#35290,#10138);
#9311=LINE('',#35292,#10139);
#9312=LINE('',#35295,#10140);
#9313=LINE('',#35297,#10141);
#9314=LINE('',#35299,#10142);
#9315=LINE('',#35301,#10143);
#9316=LINE('',#35304,#10144);
#9317=LINE('',#35306,#10145);
#9318=LINE('',#35308,#10146);
#9319=LINE('',#35322,#10147);
#9320=LINE('',#35323,#10148);
#9321=LINE('',#35328,#10149);
#9322=LINE('',#35329,#10150);
#9323=LINE('',#35343,#10151);
#9324=LINE('',#35344,#10152);
#9325=LINE('',#35349,#10153);
#9326=LINE('',#35350,#10154);
#10131=VECTOR('',#17825,1.);
#10132=VECTOR('',#17826,1.);
#10133=VECTOR('',#17827,1.);
#10134=VECTOR('',#17828,1.);
#10135=VECTOR('',#17831,1.);
#10136=VECTOR('',#17832,1.);
#10137=VECTOR('',#17833,1.);
#10138=VECTOR('',#17834,1.);
#10139=VECTOR('',#17837,1.);
#10140=VECTOR('',#17838,1.);
#10141=VECTOR('',#17839,1.);
#10142=VECTOR('',#17840,1.);
#10143=VECTOR('',#17843,1.);
#10144=VECTOR('',#17844,1.);
#10145=VECTOR('',#17845,1.);
#10146=VECTOR('',#17846,1.);
#10147=VECTOR('',#17861,1.);
#10148=VECTOR('',#17862,1.);
#10149=VECTOR('',#17867,1.);
#10150=VECTOR('',#17868,1.);
#10151=VECTOR('',#17883,1.);
#10152=VECTOR('',#17884,1.);
#10153=VECTOR('',#17889,1.);
#10154=VECTOR('',#17890,1.);
#11176=EDGE_LOOP('',(#4264,#4265,#4266,#4267));
#11177=EDGE_LOOP('',(#4268,#4269,#4270,#4271));
#11178=EDGE_LOOP('',(#4272,#4273,#4274,#4275));
#11179=EDGE_LOOP('',(#4276,#4277,#4278,#4279));
#11180=EDGE_LOOP('',(#4280,#4281,#4282,#4283));
#11181=EDGE_LOOP('',(#4284,#4285,#4286,#4287));
#11182=EDGE_LOOP('',(#4288,#4289,#4290,#4291));
#11183=EDGE_LOOP('',(#4292,#4293,#4294,#4295));
#11184=EDGE_LOOP('',(#4296,#4297,#4298,#4299));
#11185=EDGE_LOOP('',(#4300,#4301,#4302,#4303));
#11186=EDGE_LOOP('',(#4304,#4305,#4306,#4307,#4308,#4309,#4310,#4311));
#11187=EDGE_LOOP('',(#4312));
#11188=EDGE_LOOP('',(#4313,#4314,#4315,#4316));
#11189=EDGE_LOOP('',(#4317,#4318,#4319,#4320));
#11190=EDGE_LOOP('',(#4321,#4322,#4323,#4324));
#11191=EDGE_LOOP('',(#4325,#4326,#4327,#4328));
#11192=EDGE_LOOP('',(#4329,#4330,#4331,#4332));
#11193=EDGE_LOOP('',(#4333,#4334,#4335,#4336,#4337,#4338,#4339,#4340));
#11194=EDGE_LOOP('',(#4341));
#11195=EDGE_LOOP('',(#4342,#4343,#4344,#4345));
#11196=EDGE_LOOP('',(#4346,#4347,#4348,#4349));
#11197=EDGE_LOOP('',(#4350,#4351,#4352,#4353));
#11198=EDGE_LOOP('',(#4354,#4355,#4356,#4357));
#11199=EDGE_LOOP('',(#4358,#4359,#4360,#4361));
#12295=FACE_BOUND('',#11176,.T.);
#12296=FACE_BOUND('',#11177,.T.);
#12297=FACE_BOUND('',#11178,.T.);
#12298=FACE_BOUND('',#11179,.T.);
#12299=FACE_BOUND('',#11180,.T.);
#12300=FACE_BOUND('',#11181,.T.);
#12301=FACE_BOUND('',#11182,.T.);
#12302=FACE_BOUND('',#11183,.T.);
#12303=FACE_BOUND('',#11184,.T.);
#12304=FACE_BOUND('',#11185,.T.);
#12305=FACE_BOUND('',#11186,.T.);
#12306=FACE_BOUND('',#11187,.T.);
#12307=FACE_BOUND('',#11188,.T.);
#12308=FACE_BOUND('',#11189,.T.);
#12309=FACE_BOUND('',#11190,.T.);
#12310=FACE_BOUND('',#11191,.T.);
#12311=FACE_BOUND('',#11192,.T.);
#12312=FACE_BOUND('',#11193,.T.);
#12313=FACE_BOUND('',#11194,.T.);
#12314=FACE_BOUND('',#11195,.T.);
#12315=FACE_BOUND('',#11196,.T.);
#12316=FACE_BOUND('',#11197,.T.);
#12317=FACE_BOUND('',#11198,.T.);
#12318=FACE_BOUND('',#11199,.T.);
#13232=ADVANCED_FACE('',(#12295),#1423,.T.);
#13233=ADVANCED_FACE('',(#12296),#1424,.T.);
#13234=ADVANCED_FACE('',(#12297),#1425,.F.);
#13235=ADVANCED_FACE('',(#12298),#1426,.F.);
#13236=ADVANCED_FACE('',(#12299),#1427,.T.);
#13237=ADVANCED_FACE('',(#12300),#1725,.T.);
#13238=ADVANCED_FACE('',(#12301),#1726,.T.);
#13239=ADVANCED_FACE('',(#12302),#1428,.T.);
#13240=ADVANCED_FACE('',(#12303),#1727,.T.);
#13241=ADVANCED_FACE('',(#12304),#1728,.F.);
#13242=ADVANCED_FACE('',(#12305),#1429,.T.);
#13243=ADVANCED_FACE('',(#12306),#1430,.F.);
#13244=ADVANCED_FACE('',(#12307,#12308),#1431,.F.);
#13245=ADVANCED_FACE('',(#12309),#1729,.T.);
#13246=ADVANCED_FACE('',(#12310,#12311),#1432,.F.);
#13247=ADVANCED_FACE('',(#12312,#12313),#1730,.T.);
#13248=ADVANCED_FACE('',(#12314),#1731,.T.);
#13249=ADVANCED_FACE('',(#12315),#1732,.T.);
#13250=ADVANCED_FACE('',(#12316),#1733,.T.);
#13251=ADVANCED_FACE('',(#12317),#1734,.T.);
#13252=ADVANCED_FACE('',(#12318),#1735,.F.);
#13521=CLOSED_SHELL('',(#13232,#13233,#13234,#13235,#13236,#13237,#13238,
#13239,#13240,#13241,#13242,#13243,#13244,#13245,#13246,#13247,#13248,#13249,
#13250,#13251,#13252));
#13548=STYLED_ITEM('',(#13575),#13738);
#13575=PRESENTATION_STYLE_ASSIGNMENT((#13602));
#13602=SURFACE_STYLE_USAGE(.BOTH.,#13629);
#13629=SURFACE_SIDE_STYLE('',(#13656));
#13656=SURFACE_STYLE_FILL_AREA(#13683);
#13683=FILL_AREA_STYLE('',(#13710));
#13710=FILL_AREA_STYLE_COLOUR('',#60);
#13738=MANIFOLD_SOLID_BREP('refill+port_air_seal',#13521);
#13766=SHAPE_DEFINITION_REPRESENTATION(#45567,#13794);
#13794=SHAPE_REPRESENTATION('refill+port_air_seal',(#13802),#45484);
#13802=AXIS2_PLACEMENT_3D('',#19109,#15295,#15296);
#14801=AXIS2_PLACEMENT_3D('',#35273,#17823,#17824);
#14802=AXIS2_PLACEMENT_3D('',#35282,#17829,#17830);
#14803=AXIS2_PLACEMENT_3D('',#35291,#17835,#17836);
#14804=AXIS2_PLACEMENT_3D('',#35300,#17841,#17842);
#14805=AXIS2_PLACEMENT_3D('',#35309,#17847,#17848);
#14806=AXIS2_PLACEMENT_3D('',#35310,#17849,#17850);
#14807=AXIS2_PLACEMENT_3D('',#35313,#17851,#17852);
#14808=AXIS2_PLACEMENT_3D('',#35315,#17853,#17854);
#14809=AXIS2_PLACEMENT_3D('',#35317,#17855,#17856);
#14810=AXIS2_PLACEMENT_3D('',#35318,#17857,#17858);
#14811=AXIS2_PLACEMENT_3D('',#35319,#17859,#17860);
#14812=AXIS2_PLACEMENT_3D('',#35324,#17863,#17864);
#14813=AXIS2_PLACEMENT_3D('',#35325,#17865,#17866);
#14814=AXIS2_PLACEMENT_3D('',#35330,#17869,#17870);
#14815=AXIS2_PLACEMENT_3D('',#35331,#17871,#17872);
#14816=AXIS2_PLACEMENT_3D('',#35334,#17873,#17874);
#14817=AXIS2_PLACEMENT_3D('',#35336,#17875,#17876);
#14818=AXIS2_PLACEMENT_3D('',#35338,#17877,#17878);
#14819=AXIS2_PLACEMENT_3D('',#35339,#17879,#17880);
#14820=AXIS2_PLACEMENT_3D('',#35340,#17881,#17882);
#14821=AXIS2_PLACEMENT_3D('',#35345,#17885,#17886);
#14822=AXIS2_PLACEMENT_3D('',#35346,#17887,#17888);
#14823=AXIS2_PLACEMENT_3D('',#35351,#17891,#17892);
#14824=AXIS2_PLACEMENT_3D('',#35352,#17893,#17894);
#14825=AXIS2_PLACEMENT_3D('',#35353,#17895,#17896);
#14826=AXIS2_PLACEMENT_3D('',#35354,#17897,#17898);
#14827=AXIS2_PLACEMENT_3D('',#35355,#17899,#17900);
#14828=AXIS2_PLACEMENT_3D('',#35356,#17901,#17902);
#14829=AXIS2_PLACEMENT_3D('',#35357,#17903,#17904);
#14830=AXIS2_PLACEMENT_3D('',#35359,#17905,#17906);
#14831=AXIS2_PLACEMENT_3D('',#35360,#17907,#17908);
#14832=AXIS2_PLACEMENT_3D('',#35361,#17909,#17910);
#14833=AXIS2_PLACEMENT_3D('',#35362,#17911,#17912);
#14834=AXIS2_PLACEMENT_3D('',#35363,#17913,#17914);
#14835=AXIS2_PLACEMENT_3D('',#35364,#17915,#17916);
#14836=AXIS2_PLACEMENT_3D('',#35365,#17917,#17918);
#14837=AXIS2_PLACEMENT_3D('',#35366,#17919,#17920);
#14838=AXIS2_PLACEMENT_3D('',#35367,#17921,#17922);
#14839=AXIS2_PLACEMENT_3D('',#35368,#17923,#17924);
#14840=AXIS2_PLACEMENT_3D('',#35369,#17925,#17926);
#14841=AXIS2_PLACEMENT_3D('',#35370,#17927,#17928);
#14842=AXIS2_PLACEMENT_3D('',#35371,#17929,#17930);
#14843=AXIS2_PLACEMENT_3D('',#35372,#17931,#17932);
#14844=AXIS2_PLACEMENT_3D('',#35373,#17933,#17934);
#14845=AXIS2_PLACEMENT_3D('',#35374,#17935,#17936);
#14846=AXIS2_PLACEMENT_3D('',#35375,#17937,#17938);
#15295=DIRECTION('',(0.,0.,1.));
#15296=DIRECTION('',(1.,0.,0.));
#17823=DIRECTION('',(-0.573576436351044,0.819152044288994,0.));
#17824=DIRECTION('',(-0.819152044288994,-0.573576436351044,0.));
#17825=DIRECTION('',(-0.819152044288993,-0.573576436351045,0.));
#17826=DIRECTION('',(0.,0.,1.));
#17827=DIRECTION('',(0.819152044288993,0.573576436351045,0.));
#17828=DIRECTION('',(0.,0.,1.));
#17829=DIRECTION('',(0.573576436351045,0.819152044288993,0.));
#17830=DIRECTION('',(-0.819152044288993,0.573576436351045,0.));
#17831=DIRECTION('',(-0.819152044288994,0.573576436351044,0.));
#17832=DIRECTION('',(0.,0.,1.));
#17833=DIRECTION('',(0.819152044288994,-0.573576436351044,0.));
#17834=DIRECTION('',(0.,0.,1.));
#17835=DIRECTION('',(-0.573576436351044,0.819152044288994,0.));
#17836=DIRECTION('',(-0.819152044288994,-0.573576436351044,0.));
#17837=DIRECTION('',(0.819152044288994,0.573576436351044,0.));
#17838=DIRECTION('',(0.,0.,1.));
#17839=DIRECTION('',(-0.819152044288994,-0.573576436351044,0.));
#17840=DIRECTION('',(0.,0.,1.));
#17841=DIRECTION('',(0.573576436351045,0.819152044288993,0.));
#17842=DIRECTION('',(-0.819152044288993,0.573576436351045,0.));
#17843=DIRECTION('',(0.819152044288993,-0.573576436351045,0.));
#17844=DIRECTION('',(0.,0.,1.));
#17845=DIRECTION('',(-0.819152044288993,0.573576436351045,0.));
#17846=DIRECTION('',(0.,0.,1.));
#17847=DIRECTION('',(0.,0.,1.));
#17848=DIRECTION('',(1.,0.,0.));
#17849=DIRECTION('',(0.,0.,-1.));
#17850=DIRECTION('',(1.,0.,0.));
#17851=DIRECTION('',(0.,0.,-1.));
#17852=DIRECTION('',(1.,0.,0.));
#17853=DIRECTION('',(0.,0.,-1.));
#17854=DIRECTION('',(1.,0.,0.));
#17855=DIRECTION('',(0.,0.,1.));
#17856=DIRECTION('',(1.,0.,0.));
#17857=DIRECTION('',(0.,0.,-1.));
#17858=DIRECTION('',(-1.,0.,0.));
#17859=DIRECTION('',(0.,0.,-1.));
#17860=DIRECTION('',(1.,0.,0.));
#17861=DIRECTION('',(0.,0.,-1.));
#17862=DIRECTION('',(0.,0.,-1.));
#17863=DIRECTION('',(0.,0.,-1.));
#17864=DIRECTION('',(-1.,0.,0.));
#17865=DIRECTION('',(0.,0.,-1.));
#17866=DIRECTION('',(1.,0.,0.));
#17867=DIRECTION('',(0.,0.,-1.));
#17868=DIRECTION('',(0.,0.,-1.));
#17869=DIRECTION('',(0.,0.,1.));
#17870=DIRECTION('',(1.,0.,0.));
#17871=DIRECTION('',(0.,0.,-1.));
#17872=DIRECTION('',(-1.,0.,0.));
#17873=DIRECTION('',(0.,0.,1.));
#17874=DIRECTION('',(-1.,0.,0.));
#17875=DIRECTION('',(0.,0.,-1.));
#17876=DIRECTION('',(-1.,0.,0.));
#17877=DIRECTION('',(0.,0.,-1.));
#17878=DIRECTION('',(-1.,0.,0.));
#17879=DIRECTION('',(0.,0.,-1.));
#17880=DIRECTION('',(-1.,0.,0.));
#17881=DIRECTION('',(0.,0.,-1.));
#17882=DIRECTION('',(-1.,0.,0.));
#17883=DIRECTION('',(0.,0.,-1.));
#17884=DIRECTION('',(0.,0.,-1.));
#17885=DIRECTION('',(0.,0.,-1.));
#17886=DIRECTION('',(-1.,0.,0.));
#17887=DIRECTION('',(0.,0.,1.));
#17888=DIRECTION('',(-1.,0.,0.));
#17889=DIRECTION('',(0.,0.,-1.));
#17890=DIRECTION('',(0.,0.,-1.));
#17891=DIRECTION('',(0.,0.,-1.));
#17892=DIRECTION('',(-1.,0.,0.));
#17893=DIRECTION('',(0.,0.,1.));
#17894=DIRECTION('',(-1.,0.,0.));
#17895=DIRECTION('',(0.,0.,-1.));
#17896=DIRECTION('',(-1.,0.,0.));
#17897=DIRECTION('',(0.,0.,1.));
#17898=DIRECTION('',(-1.,0.,0.));
#17899=DIRECTION('',(0.,0.,-1.));
#17900=DIRECTION('',(-1.,0.,0.));
#17901=DIRECTION('',(0.,0.,-1.));
#17902=DIRECTION('',(-1.,0.,0.));
#17903=DIRECTION('',(0.,0.,-1.));
#17904=DIRECTION('',(-1.,0.,0.));
#17905=DIRECTION('',(0.,0.,-1.));
#17906=DIRECTION('',(-1.,0.,0.));
#17907=DIRECTION('',(0.,0.,-1.));
#17908=DIRECTION('',(-1.,0.,0.));
#17909=DIRECTION('',(0.,0.,-1.));
#17910=DIRECTION('',(-1.,0.,0.));
#17911=DIRECTION('',(0.,0.,-1.));
#17912=DIRECTION('',(-1.,0.,0.));
#17913=DIRECTION('',(0.,0.,-1.));
#17914=DIRECTION('',(-1.,0.,0.));
#17915=DIRECTION('',(0.,0.,1.));
#17916=DIRECTION('',(1.,0.,0.));
#17917=DIRECTION('',(0.,0.,-1.));
#17918=DIRECTION('',(-1.,0.,0.));
#17919=DIRECTION('',(0.,0.,-1.));
#17920=DIRECTION('',(-1.,0.,0.));
#17921=DIRECTION('',(0.,0.,-1.));
#17922=DIRECTION('',(-1.,0.,0.));
#17923=DIRECTION('',(0.,0.,-1.));
#17924=DIRECTION('',(1.,0.,0.));
#17925=DIRECTION('',(0.,0.,1.));
#17926=DIRECTION('',(1.,0.,0.));
#17927=DIRECTION('',(0.,0.,-1.));
#17928=DIRECTION('',(-1.,0.,0.));
#17929=DIRECTION('',(0.,0.,1.));
#17930=DIRECTION('',(1.,0.,0.));
#17931=DIRECTION('',(0.,0.,-1.));
#17932=DIRECTION('',(-1.,0.,0.));
#17933=DIRECTION('',(0.,0.,-1.));
#17934=DIRECTION('',(-1.,0.,0.));
#17935=DIRECTION('',(0.,0.,-1.));
#17936=DIRECTION('',(-1.,0.,0.));
#17937=DIRECTION('',(0.,0.,-1.));
#17938=DIRECTION('',(-1.,0.,0.));
#19109=CARTESIAN_POINT('',(0.,0.,0.));
#35273=CARTESIAN_POINT('',(-0.012319152044289,0.0297373126961043,0.011));
#35274=CARTESIAN_POINT('',(-0.0115,0.0303108891324553,0.018));
#35275=CARTESIAN_POINT('',(-0.00863296784498857,0.032318406659684,0.018));
#35276=CARTESIAN_POINT('',(-0.010680847955711,0.0308844655688064,0.018));
#35277=CARTESIAN_POINT('',(-0.010680847955711,0.0308844655688064,0.011));
#35278=CARTESIAN_POINT('',(-0.010680847955711,0.0308844655688064,0.021));
#35279=CARTESIAN_POINT('',(-0.010680847955711,0.0308844655688064,0.021));
#35280=CARTESIAN_POINT('',(-0.00863296784498857,0.032318406659684,0.021));
#35281=CARTESIAN_POINT('',(-0.00863296784498857,0.032318406659684,0.011));
#35282=CARTESIAN_POINT('',(-0.010680847955711,0.0297373126961043,0.011));
#35283=CARTESIAN_POINT('',(-0.0115,0.0303108891324553,0.018));
#35284=CARTESIAN_POINT('',(-0.012319152044289,0.0308844655688064,0.018));
#35285=CARTESIAN_POINT('',(-0.0143670321550115,0.032318406659684,0.018));
#35286=CARTESIAN_POINT('',(-0.0143670321550115,0.032318406659684,0.011));
#35287=CARTESIAN_POINT('',(-0.0143670321550115,0.032318406659684,0.021));
#35288=CARTESIAN_POINT('',(-0.012319152044289,0.0308844655688064,0.021));
#35289=CARTESIAN_POINT('',(-0.012319152044289,0.0308844655688064,0.021));
#35290=CARTESIAN_POINT('',(-0.012319152044289,0.0308844655688064,0.011));
#35291=CARTESIAN_POINT('',(-0.012319152044289,0.0297373126961043,0.011));
#35292=CARTESIAN_POINT('',(-0.0115,0.0303108891324553,0.018));
#35293=CARTESIAN_POINT('',(-0.0143670321550115,0.0283033716052267,0.018));
#35294=CARTESIAN_POINT('',(-0.012319152044289,0.0297373126961043,0.018));
#35295=CARTESIAN_POINT('',(-0.012319152044289,0.0297373126961043,0.011));
#35296=CARTESIAN_POINT('',(-0.012319152044289,0.0297373126961043,0.021));
#35297=CARTESIAN_POINT('',(-0.012319152044289,0.0297373126961043,0.021));
#35298=CARTESIAN_POINT('',(-0.0143670321550115,0.0283033716052267,0.021));
#35299=CARTESIAN_POINT('',(-0.0143670321550115,0.0283033716052267,0.011));
#35300=CARTESIAN_POINT('',(-0.010680847955711,0.0297373126961043,0.011));
#35301=CARTESIAN_POINT('',(-0.0115,0.0303108891324553,0.018));
#35302=CARTESIAN_POINT('',(-0.010680847955711,0.0297373126961043,0.018));
#35303=CARTESIAN_POINT('',(-0.00863296784498857,0.0283033716052267,0.018));
#35304=CARTESIAN_POINT('',(-0.00863296784498857,0.0283033716052267,0.011));
#35305=CARTESIAN_POINT('',(-0.00863296784498857,0.0283033716052267,0.021));
#35306=CARTESIAN_POINT('',(-0.010680847955711,0.0297373126961043,0.021));
#35307=CARTESIAN_POINT('',(-0.010680847955711,0.0297373126961043,0.021));
#35308=CARTESIAN_POINT('',(-0.010680847955711,0.0297373126961043,0.011));
#35309=CARTESIAN_POINT('',(-0.012852081728299,0.0305608891324553,0.026));
#35310=CARTESIAN_POINT('',(-0.014204163456598,0.0308108891324553,0.026));
#35311=CARTESIAN_POINT('',(-0.0146732429566961,0.0308976219627052,0.026));
#35312=CARTESIAN_POINT('',(-0.0137350839565,0.0307241563022055,0.026));
#35313=CARTESIAN_POINT('',(-0.0115,0.0303108891324553,0.026));
#35314=CARTESIAN_POINT('',(-0.0146732429566961,0.0297241563022054,0.026));
#35315=CARTESIAN_POINT('',(-0.014204163456598,0.0298108891324554,0.026));
#35316=CARTESIAN_POINT('',(-0.0137350839565,0.0298976219627052,0.026));
#35317=CARTESIAN_POINT('',(-0.0115,0.0303108891324553,0.026));
#35318=CARTESIAN_POINT('',(-0.014204163456598,0.0298108891324554,0.026));
#35319=CARTESIAN_POINT('',(-0.014204163456598,0.0298108891324554,0.021));
#35320=CARTESIAN_POINT('',(-0.0137350839565,0.0298976219627052,0.021));
#35321=CARTESIAN_POINT('',(-0.0146732429566961,0.0297241563022054,0.021));
#35322=CARTESIAN_POINT('',(-0.0137350839565,0.0298976219627052,0.026));
#35323=CARTESIAN_POINT('',(-0.0146732429566961,0.0297241563022054,0.026));
#35324=CARTESIAN_POINT('',(-0.014204163456598,0.0308108891324553,0.026));
#35325=CARTESIAN_POINT('',(-0.014204163456598,0.0308108891324553,0.021));
#35326=CARTESIAN_POINT('',(-0.0146732429566961,0.0308976219627052,0.021));
#35327=CARTESIAN_POINT('',(-0.0137350839565,0.0307241563022055,0.021));
#35328=CARTESIAN_POINT('',(-0.0146732429566961,0.0308976219627052,0.026));
#35329=CARTESIAN_POINT('',(-0.0137350839565,0.0307241563022055,0.026));
#35330=CARTESIAN_POINT('',(-0.012852081728299,0.0305608891324553,0.026));
#35331=CARTESIAN_POINT('',(-0.00879583654340205,0.0308108891324553,0.026));
#35332=CARTESIAN_POINT('',(-0.0092649160435001,0.0307241563022055,0.026));
#35333=CARTESIAN_POINT('',(-0.008326757043304,0.0308976219627052,0.026));
#35334=CARTESIAN_POINT('',(-0.0115,0.0303108891324553,0.026));
#35335=CARTESIAN_POINT('',(-0.0092649160435001,0.0298976219627052,0.026));
#35336=CARTESIAN_POINT('',(-0.00879583654340205,0.0298108891324554,0.026));
#35337=CARTESIAN_POINT('',(-0.00832675704330399,0.0297241563022054,0.026));
#35338=CARTESIAN_POINT('',(-0.0115,0.0303108891324553,0.026));
#35339=CARTESIAN_POINT('',(-0.0115,0.0303108891324553,0.026));
#35340=CARTESIAN_POINT('',(-0.0115,0.0303108891324553,0.021));
#35341=CARTESIAN_POINT('',(-0.00832675704330399,0.0308976219627052,0.021));
#35342=CARTESIAN_POINT('',(-0.008326757043304,0.0297241563022054,0.021));
#35343=CARTESIAN_POINT('',(-0.008326757043304,0.0308976219627052,0.026));
#35344=CARTESIAN_POINT('',(-0.008326757043304,0.0297241563022054,0.026));
#35345=CARTESIAN_POINT('',(-0.0115,0.0303108891324553,0.026));
#35346=CARTESIAN_POINT('',(-0.0115,0.0303108891324553,0.021));
#35347=CARTESIAN_POINT('',(-0.0092649160435001,0.0298976219627052,0.021));
#35348=CARTESIAN_POINT('',(-0.0092649160435001,0.0307241563022055,0.021));
#35349=CARTESIAN_POINT('',(-0.0092649160435001,0.0298976219627052,0.026));
#35350=CARTESIAN_POINT('',(-0.0092649160435001,0.0307241563022055,0.026));
#35351=CARTESIAN_POINT('',(-0.0115,0.0303108891324553,0.018));
#35352=CARTESIAN_POINT('',(-0.0115,0.0303108891324553,0.018));
#35353=CARTESIAN_POINT('',(-0.0115,0.0303108891324553,0.018));
#35354=CARTESIAN_POINT('',(-0.0115,0.0303108891324553,0.018));
#35355=CARTESIAN_POINT('',(-0.0115,0.0303108891324553,0.018));
#35356=CARTESIAN_POINT('',(0.,0.,0.025));
#35357=CARTESIAN_POINT('',(-0.0115,0.0303108891324553,0.025));
#35358=CARTESIAN_POINT('',(-0.0125,0.0303108891324553,0.025));
#35359=CARTESIAN_POINT('',(-0.0115,0.0303108891324553,0.021));
#35360=CARTESIAN_POINT('',(-0.0115,0.0303108891324553,0.021));
#35361=CARTESIAN_POINT('',(-0.0115,0.0303108891324553,0.021));
#35362=CARTESIAN_POINT('',(-0.00879583654340205,0.0308108891324553,0.021));
#35363=CARTESIAN_POINT('',(-0.00879583654340205,0.0298108891324554,0.021));
#35364=CARTESIAN_POINT('',(-0.0115,0.0303108891324553,0.018));
#35365=CARTESIAN_POINT('',(-0.0115,0.0303108891324553,0.021));
#35366=CARTESIAN_POINT('',(-0.0115,0.0303108891324553,0.021));
#35367=CARTESIAN_POINT('',(-0.0115,0.0303108891324553,0.021));
#35368=CARTESIAN_POINT('',(-0.0115,0.0303108891324553,0.021));
#35369=CARTESIAN_POINT('',(-0.0115,0.0303108891324553,0.021));
#35370=CARTESIAN_POINT('',(-0.0115,0.0303108891324553,0.025));
#35371=CARTESIAN_POINT('',(-0.0115,0.0303108891324553,0.018));
#35372=CARTESIAN_POINT('',(-0.00879583654340205,0.0308108891324553,0.026));
#35373=CARTESIAN_POINT('',(-0.00879583654340205,0.0298108891324554,0.026));
#35374=CARTESIAN_POINT('',(-0.0115,0.0303108891324553,0.026));
#35375=CARTESIAN_POINT('',(-0.0115,0.0303108891324553,0.026));
#45463=MECHANICAL_DESIGN_GEOMETRIC_PRESENTATION_REPRESENTATION('',(#13548),#45464);
#45464=(
GEOMETRIC_REPRESENTATION_CONTEXT(3)
GLOBAL_UNCERTAINTY_ASSIGNED_CONTEXT((#45492))
GLOBAL_UNIT_ASSIGNED_CONTEXT((#45522,#45521,#45520))
REPRESENTATION_CONTEXT('MAS-690','TOP_LEVEL_ASSEMBLY_PART')
);
#45484=(
GEOMETRIC_REPRESENTATION_CONTEXT(3)
GLOBAL_UNCERTAINTY_ASSIGNED_CONTEXT((#45512))
GLOBAL_UNIT_ASSIGNED_CONTEXT((#45522,#45521,#45520))
REPRESENTATION_CONTEXT('refill+port_air_seal','COMPONENT_PART')
);
#45492=UNCERTAINTY_MEASURE_WITH_UNIT(LENGTH_MEASURE(1.E-8),#45522,
'DISTANCE_ACCURACY_VALUE','Maximum Tolerance applied to model');
#45512=UNCERTAINTY_MEASURE_WITH_UNIT(LENGTH_MEASURE(1.E-6),#45522,
'DISTANCE_ACCURACY_VALUE','Maximum Tolerance applied to model');
#45520=(
NAMED_UNIT(*)
SI_UNIT($,.STERADIAN.)
SOLID_ANGLE_UNIT()
);
#45521=(
NAMED_UNIT(*)
PLANE_ANGLE_UNIT()
SI_UNIT($,.RADIAN.)
);
#45522=(
LENGTH_UNIT()
NAMED_UNIT(*)
SI_UNIT($,.METRE.)
);
#45567=PRODUCT_DEFINITION_SHAPE('','',#45605);
#45605=PRODUCT_DEFINITION('','',#45661,#45633);
#45633=PRODUCT_DEFINITION_CONTEXT('',#45782,'design');
#45661=PRODUCT_DEFINITION_FORMATION_WITH_SPECIFIED_SOURCE('','',#45717,
 .NOT_KNOWN.);
#45717=PRODUCT('refill+port_air_seal','refill+port_air_seal',
'refill+port_air_seal',(#45773));
#45773=PRODUCT_CONTEXT('',#45782,'mechanical');
#45782=APPLICATION_CONTEXT('managed model based 3d engineering');
ENDSEC;
END-ISO-10303-21;
